ISO-10303-21;
HEADER;
/* Generated by software containing ST-Developer
 * from STEP Tools, Inc. (www.steptools.com) 
 */
/* OPTION: using custom renumber hook */

FILE_DESCRIPTION(
/* description */ ('STEP AP242 Edition 2', 'CAx-IF Rec.Pracs.---Representation and Presentation of Product Manufa
cturing Information (PMI)---4.0---2014-10-13', 'CAx-IF Rec.Pracs.---3D Tessellated Geometry---0.4---2014-09-14', '2;1', 'CAx-IF Rec.Pracs.---User Defined Attributes---1.5---2016-08-15'),
/* implementation_level */ '2;1');

FILE_NAME(
/* name */ 'Part 2__PD8598.step',
/* time_stamp */ '2026-10-07T00:00:55Z',
/* author */ (''),
/* organization */ (''),
/* preprocessor_version */ 'ST-DEVELOPER v20',
/* originating_system */ 'ONSHAPE BY PTC INC, 1.221',
/* authorisation */ '  ');

FILE_SCHEMA (('AP242_MANAGED_MODEL_BASED_3D_ENGINEERING_MIM_LF { 1 0 10303 442 3 1 4 }'));
ENDSEC;

DATA;
#125=SHAPE_REPRESENTATION_RELATIONSHIP('','',#4481,#136);
#136=ADVANCED_BREP_SHAPE_REPRESENTATION('',(#4457),#8544);
#279=CYLINDRICAL_SURFACE('',#4952,0.01);
#280=CYLINDRICAL_SURFACE('',#4955,0.011);
#544=CIRCLE('',#4953,0.01);
#545=CIRCLE('',#4954,0.01);
#546=CIRCLE('',#4956,0.011);
#547=CIRCLE('',#4957,0.011);
#1627=ORIENTED_EDGE('',*,*,#2333,.T.);
#1628=ORIENTED_EDGE('',*,*,#2334,.F.);
#1629=ORIENTED_EDGE('',*,*,#2335,.F.);
#1630=ORIENTED_EDGE('',*,*,#2336,.T.);
#1631=ORIENTED_EDGE('',*,*,#2333,.F.);
#1632=ORIENTED_EDGE('',*,*,#2335,.T.);
#1633=ORIENTED_EDGE('',*,*,#2334,.T.);
#1634=ORIENTED_EDGE('',*,*,#2336,.F.);
#2333=EDGE_CURVE('',#2748,#2748,#544,.T.);
#2334=EDGE_CURVE('',#2749,#2749,#545,.T.);
#2335=EDGE_CURVE('',#2750,#2750,#546,.T.);
#2336=EDGE_CURVE('',#2751,#2751,#547,.T.);
#2748=VERTEX_POINT('',#8058);
#2749=VERTEX_POINT('',#8060);
#2750=VERTEX_POINT('',#8063);
#2751=VERTEX_POINT('',#8065);
#3482=EDGE_LOOP('',(#1627));
#3483=EDGE_LOOP('',(#1628));
#3484=EDGE_LOOP('',(#1629));
#3485=EDGE_LOOP('',(#1630));
#3486=EDGE_LOOP('',(#1631));
#3487=EDGE_LOOP('',(#1632));
#3488=EDGE_LOOP('',(#1633));
#3489=EDGE_LOOP('',(#1634));
#3859=FACE_BOUND('',#3482,.T.);
#3860=FACE_BOUND('',#3483,.T.);
#3861=FACE_BOUND('',#3484,.T.);
#3862=FACE_BOUND('',#3485,.T.);
#3863=FACE_BOUND('',#3486,.T.);
#3864=FACE_BOUND('',#3487,.T.);
#3865=FACE_BOUND('',#3488,.T.);
#3866=FACE_BOUND('',#3489,.T.);
#4012=PLANE('',#4958);
#4013=PLANE('',#4959);
#4266=ADVANCED_FACE('',(#3859,#3860),#279,.F.);
#4267=ADVANCED_FACE('',(#3861,#3862),#280,.T.);
#4268=ADVANCED_FACE('',(#3863,#3864),#4012,.T.);
#4269=ADVANCED_FACE('',(#3865,#3866),#4013,.F.);
#4331=CLOSED_SHELL('',(#4266,#4267,#4268,#4269));
#4342=STYLED_ITEM('',(#4353),#4457);
#4353=PRESENTATION_STYLE_ASSIGNMENT((#4369));
#4369=SURFACE_STYLE_USAGE(.BOTH.,#4385);
#4385=SURFACE_SIDE_STYLE('',(#4401));
#4401=SURFACE_STYLE_FILL_AREA(#4417);
#4417=FILL_AREA_STYLE('',(#4433));
#4433=FILL_AREA_STYLE_COLOUR('',#4446);
#4446=COLOUR_RGB('', 0.40784314, 0.44705882, 0.49803922);
#4457=MANIFOLD_SOLID_BREP('Part 2',#4331);
#4469=SHAPE_DEFINITION_REPRESENTATION(#8582,#4481);
#4481=SHAPE_REPRESENTATION('Part 2',(#4484),#8544);
#4484=AXIS2_PLACEMENT_3D('',#6402,#5064,#5065);
#4952=AXIS2_PLACEMENT_3D('',#8056,#6134,#6135);
#4953=AXIS2_PLACEMENT_3D('',#8057,#6136,#6137);
#4954=AXIS2_PLACEMENT_3D('',#8059,#6138,#6139);
#4955=AXIS2_PLACEMENT_3D('',#8061,#6140,#6141);
#4956=AXIS2_PLACEMENT_3D('',#8062,#6142,#6143);
#4957=AXIS2_PLACEMENT_3D('',#8064,#6144,#6145);
#4958=AXIS2_PLACEMENT_3D('',#8066,#6146,#6147);
#4959=AXIS2_PLACEMENT_3D('',#8067,#6148,#6149);
#5064=DIRECTION('',(0.,0.,1.));
#5065=DIRECTION('',(1.,0.,0.));
#6134=DIRECTION('',(0.,0.,-1.));
#6135=DIRECTION('',(-1.,0.,0.));
#6136=DIRECTION('',(0.,0.,1.));
#6137=DIRECTION('',(1.,-6.12323399573677E-17,0.));
#6138=DIRECTION('',(0.,0.,1.));
#6139=DIRECTION('',(1.,-6.12323399573677E-17,0.));
#6140=DIRECTION('',(0.,0.,-1.));
#6141=DIRECTION('',(-1.,0.,0.));
#6142=DIRECTION('',(0.,0.,1.));
#6143=DIRECTION('',(1.,-6.12323399573677E-17,0.));
#6144=DIRECTION('',(0.,0.,1.));
#6145=DIRECTION('',(1.,-6.12323399573677E-17,0.));
#6146=DIRECTION('',(0.,0.,1.));
#6147=DIRECTION('',(1.,0.,0.));
#6148=DIRECTION('',(0.,0.,1.));
#6149=DIRECTION('',(1.,0.,0.));
#6402=CARTESIAN_POINT('',(0.,0.,0.));
#8056=CARTESIAN_POINT('',(0.,6.12323399573677E-19,0.0125));
#8057=CARTESIAN_POINT('',(0.,6.12323399573677E-19,0.0125));
#8058=CARTESIAN_POINT('',(0.01,9.62964972193618E-35,0.0125));
#8059=CARTESIAN_POINT('',(0.,6.12323399573677E-19,-0.0125));
#8060=CARTESIAN_POINT('',(0.01,9.62964972193618E-35,-0.0125));
#8061=CARTESIAN_POINT('',(0.,6.73555739531044E-19,0.0125));
#8062=CARTESIAN_POINT('',(0.,6.73555739531044E-19,0.0125));
#8063=CARTESIAN_POINT('',(0.011,-6.74075480535533E-34,0.0125));
#8064=CARTESIAN_POINT('',(0.,6.73555739531044E-19,-0.0125));
#8065=CARTESIAN_POINT('',(0.011,-6.74075480535533E-34,-0.0125));
#8066=CARTESIAN_POINT('',(0.,0.,0.0125));
#8067=CARTESIAN_POINT('',(0.,0.,-0.0125));
#8534=MECHANICAL_DESIGN_GEOMETRIC_PRESENTATION_REPRESENTATION('',(#4342),#8535);
#8535=(
GEOMETRIC_REPRESENTATION_CONTEXT(3)
GLOBAL_UNCERTAINTY_ASSIGNED_CONTEXT((#8547))
GLOBAL_UNIT_ASSIGNED_CONTEXT((#8561,#8560,#8559))
REPRESENTATION_CONTEXT('MAS-680','TOP_LEVEL_ASSEMBLY_PART')
);
#8544=(
GEOMETRIC_REPRESENTATION_CONTEXT(3)
GLOBAL_UNCERTAINTY_ASSIGNED_CONTEXT((#8556))
GLOBAL_UNIT_ASSIGNED_CONTEXT((#8561,#8560,#8559))
REPRESENTATION_CONTEXT('Part 2','COMPONENT_PART')
);
#8547=UNCERTAINTY_MEASURE_WITH_UNIT(LENGTH_MEASURE(1.E-8),#8561,
'DISTANCE_ACCURACY_VALUE','Maximum Tolerance applied to model');
#8556=UNCERTAINTY_MEASURE_WITH_UNIT(LENGTH_MEASURE(1.E-8),#8561,
'DISTANCE_ACCURACY_VALUE','Maximum Tolerance applied to model');
#8559=(
NAMED_UNIT(*)
SI_UNIT($,.STERADIAN.)
SOLID_ANGLE_UNIT()
);
#8560=(
NAMED_UNIT(*)
PLANE_ANGLE_UNIT()
SI_UNIT($,.RADIAN.)
);
#8561=(
LENGTH_UNIT()
NAMED_UNIT(*)
SI_UNIT($,.METRE.)
);
#8582=PRODUCT_DEFINITION_SHAPE('','',#8598);
#8598=PRODUCT_DEFINITION('','',#8622,#8610);
#8610=PRODUCT_DEFINITION_CONTEXT('',#8674,'design');
#8622=PRODUCT_DEFINITION_FORMATION_WITH_SPECIFIED_SOURCE('','',#8646,
 .NOT_KNOWN.);
#8646=PRODUCT('Part 2','Part 2','Part 2',(#8670));
#8670=PRODUCT_CONTEXT('',#8674,'mechanical');
#8674=APPLICATION_CONTEXT('managed model based 3d engineering');
ENDSEC;
END-ISO-10303-21;
